ISO-10303-21;
HEADER;
/* Generated by software containing ST-Developer
 * from STEP Tools, Inc. (www.steptools.com) 
 */

FILE_DESCRIPTION(
/* description */ ('Manual rail carriage with stops'),
/* implementation_level */ '2;1');

FILE_NAME(
/* name */ 'M5x14 Cap Screw.step',
/* time_stamp */ '2026-10-27T18:54:27-07:00',
/* author */ (''),
/* organization */ (''),
/* preprocessor_version */ 'ST-DEVELOPER v20.2',
/* originating_system */ 'Autodesk Translation Framework v15.17.0.0',
/* authorisation */ '');

FILE_SCHEMA (('AUTOMOTIVE_DESIGN { 1 0 10303 214 3 1 1 }'));
ENDSEC;

DATA;
#10=MECHANICAL_DESIGN_GEOMETRIC_PRESENTATION_REPRESENTATION('',(#276),#8499);
#211=CONICAL_SURFACE('',#5297,0.4,0.785398163397448);
#212=CONICAL_SURFACE('',#5301,0.41,0.785398163397448);
#213=CONICAL_SURFACE('',#5305,0.26,0.463647609000806);
#227=ORIENTED_CLOSED_SHELL('',*,#4944,.F.);
#231=BREP_WITH_VOIDS('Body1',#4945,(#227));
#240=SHAPE_REPRESENTATION_RELATIONSHIP('SRR','None',#8603,#258);
#258=ADVANCED_BREP_SHAPE_REPRESENTATION('',(#231),#8482);
#276=STYLED_ITEM('',(#8795),#231);
#336=FACE_BOUND('',#968,.T.);
#445=PLANE('',#5285);
#446=PLANE('',#5286);
#447=PLANE('',#5287);
#448=PLANE('',#5288);
#449=PLANE('',#5289);
#450=PLANE('',#5290);
#451=PLANE('',#5291);
#452=PLANE('',#5292);
#453=PLANE('',#5293);
#454=PLANE('',#5295);
#455=PLANE('',#5303);
#658=FACE_OUTER_BOUND('',#954,.T.);
#659=FACE_OUTER_BOUND('',#955,.T.);
#660=FACE_OUTER_BOUND('',#956,.T.);
#661=FACE_OUTER_BOUND('',#957,.T.);
#662=FACE_OUTER_BOUND('',#958,.T.);
#663=FACE_OUTER_BOUND('',#959,.T.);
#664=FACE_OUTER_BOUND('',#960,.T.);
#665=FACE_OUTER_BOUND('',#961,.T.);
#666=FACE_OUTER_BOUND('',#962,.T.);
#667=FACE_OUTER_BOUND('',#963,.T.);
#668=FACE_OUTER_BOUND('',#964,.T.);
#669=FACE_OUTER_BOUND('',#965,.T.);
#670=FACE_OUTER_BOUND('',#966,.T.);
#671=FACE_OUTER_BOUND('',#967,.T.);
#672=FACE_OUTER_BOUND('',#969,.T.);
#673=FACE_OUTER_BOUND('',#970,.T.);
#954=EDGE_LOOP('',(#3816,#3817,#3818,#3819));
#955=EDGE_LOOP('',(#3820,#3821,#3822,#3823));
#956=EDGE_LOOP('',(#3824,#3825,#3826,#3827));
#957=EDGE_LOOP('',(#3828,#3829,#3830,#3831));
#958=EDGE_LOOP('',(#3832,#3833,#3834,#3835));
#959=EDGE_LOOP('',(#3836,#3837,#3838,#3839));
#960=EDGE_LOOP('',(#3840,#3841,#3842,#3843,#3844,#3845));
#961=EDGE_LOOP('',(#3846,#3847,#3848,#3849,#3850,#3851));
#962=EDGE_LOOP('',(#3852));
#963=EDGE_LOOP('',(#3853));
#964=EDGE_LOOP('',(#3854,#3855,#3856,#3857));
#965=EDGE_LOOP('',(#3858,#3859,#3860,#3861));
#966=EDGE_LOOP('',(#3862,#3863,#3864,#3865));
#967=EDGE_LOOP('',(#3866));
#968=EDGE_LOOP('',(#3867));
#969=EDGE_LOOP('',(#3868,#3869,#3870,#3871));
#970=EDGE_LOOP('',(#3872,#3873,#3874,#3875));
#1374=LINE('',#7539,#1874);
#1375=LINE('',#7541,#1875);
#1376=LINE('',#7543,#1876);
#1377=LINE('',#7544,#1877);
#1378=LINE('',#7547,#1878);
#1379=LINE('',#7549,#1879);
#1380=LINE('',#7550,#1880);
#1381=LINE('',#7553,#1881);
#1382=LINE('',#7555,#1882);
#1383=LINE('',#7556,#1883);
#1384=LINE('',#7559,#1884);
#1385=LINE('',#7561,#1885);
#1386=LINE('',#7562,#1886);
#1387=LINE('',#7565,#1887);
#1388=LINE('',#7567,#1888);
#1389=LINE('',#7568,#1889);
#1390=LINE('',#7570,#1890);
#1391=LINE('',#7571,#1891);
#1392=LINE('',#7583,#1892);
#1393=LINE('',#7587,#1893);
#1394=LINE('',#7591,#1894);
#1395=LINE('',#7598,#1895);
#1396=LINE('',#7600,#1896);
#1874=VECTOR('',#6071,1.);
#1875=VECTOR('',#6072,1.);
#1876=VECTOR('',#6073,1.);
#1877=VECTOR('',#6074,1.);
#1878=VECTOR('',#6077,1.);
#1879=VECTOR('',#6078,1.);
#1880=VECTOR('',#6079,1.);
#1881=VECTOR('',#6082,1.);
#1882=VECTOR('',#6083,1.);
#1883=VECTOR('',#6084,1.);
#1884=VECTOR('',#6087,1.);
#1885=VECTOR('',#6088,1.);
#1886=VECTOR('',#6089,1.);
#1887=VECTOR('',#6092,1.);
#1888=VECTOR('',#6093,1.);
#1889=VECTOR('',#6094,1.);
#1890=VECTOR('',#6097,1.);
#1891=VECTOR('',#6098,1.);
#1892=VECTOR('',#6115,0.4);
#1893=VECTOR('',#6120,0.425);
#1894=VECTOR('',#6125,0.41);
#1895=VECTOR('',#6134,0.26);
#1896=VECTOR('',#6137,0.25);
#2216=CIRCLE('',#5294,0.24505);
#2217=CIRCLE('',#5296,0.375);
#2218=CIRCLE('',#5298,0.425);
#2219=CIRCLE('',#5300,0.425);
#2220=CIRCLE('',#5302,0.395);
#2221=CIRCLE('',#5304,0.27);
#2222=CIRCLE('',#5306,0.24505);
#2464=VERTEX_POINT('',#7537);
#2465=VERTEX_POINT('',#7538);
#2466=VERTEX_POINT('',#7540);
#2467=VERTEX_POINT('',#7542);
#2468=VERTEX_POINT('',#7546);
#2469=VERTEX_POINT('',#7548);
#2470=VERTEX_POINT('',#7552);
#2471=VERTEX_POINT('',#7554);
#2472=VERTEX_POINT('',#7558);
#2473=VERTEX_POINT('',#7560);
#2474=VERTEX_POINT('',#7564);
#2475=VERTEX_POINT('',#7566);
#2476=VERTEX_POINT('',#7575);
#2477=VERTEX_POINT('',#7578);
#2478=VERTEX_POINT('',#7581);
#2479=VERTEX_POINT('',#7585);
#2480=VERTEX_POINT('',#7589);
#2481=VERTEX_POINT('',#7593);
#2482=VERTEX_POINT('',#7596);
#2956=EDGE_CURVE('',#2464,#2465,#1374,.T.);
#2957=EDGE_CURVE('',#2465,#2466,#1375,.T.);
#2958=EDGE_CURVE('',#2466,#2467,#1376,.T.);
#2959=EDGE_CURVE('',#2464,#2467,#1377,.T.);
#2960=EDGE_CURVE('',#2465,#2468,#1378,.T.);
#2961=EDGE_CURVE('',#2468,#2469,#1379,.T.);
#2962=EDGE_CURVE('',#2469,#2466,#1380,.T.);
#2963=EDGE_CURVE('',#2468,#2470,#1381,.T.);
#2964=EDGE_CURVE('',#2470,#2471,#1382,.T.);
#2965=EDGE_CURVE('',#2471,#2469,#1383,.T.);
#2966=EDGE_CURVE('',#2470,#2472,#1384,.T.);
#2967=EDGE_CURVE('',#2472,#2473,#1385,.T.);
#2968=EDGE_CURVE('',#2473,#2471,#1386,.T.);
#2969=EDGE_CURVE('',#2472,#2474,#1387,.T.);
#2970=EDGE_CURVE('',#2474,#2475,#1388,.T.);
#2971=EDGE_CURVE('',#2475,#2473,#1389,.T.);
#2972=EDGE_CURVE('',#2474,#2464,#1390,.T.);
#2973=EDGE_CURVE('',#2467,#2475,#1391,.T.);
#2974=EDGE_CURVE('',#2476,#2476,#2216,.T.);
#2975=EDGE_CURVE('',#2477,#2477,#2217,.T.);
#2976=EDGE_CURVE('',#2478,#2478,#2218,.T.);
#2977=EDGE_CURVE('',#2478,#2477,#1392,.T.);
#2978=EDGE_CURVE('',#2479,#2479,#2219,.T.);
#2979=EDGE_CURVE('',#2479,#2478,#1393,.T.);
#2980=EDGE_CURVE('',#2480,#2480,#2220,.T.);
#2981=EDGE_CURVE('',#2480,#2479,#1394,.T.);
#2982=EDGE_CURVE('',#2481,#2481,#2221,.T.);
#2983=EDGE_CURVE('',#2482,#2482,#2222,.F.);
#2984=EDGE_CURVE('',#2482,#2481,#1395,.T.);
#2985=EDGE_CURVE('',#2476,#2482,#1396,.T.);
#3816=ORIENTED_EDGE('',*,*,#2956,.T.);
#3817=ORIENTED_EDGE('',*,*,#2957,.T.);
#3818=ORIENTED_EDGE('',*,*,#2958,.T.);
#3819=ORIENTED_EDGE('',*,*,#2959,.F.);
#3820=ORIENTED_EDGE('',*,*,#2960,.T.);
#3821=ORIENTED_EDGE('',*,*,#2961,.T.);
#3822=ORIENTED_EDGE('',*,*,#2962,.T.);
#3823=ORIENTED_EDGE('',*,*,#2957,.F.);
#3824=ORIENTED_EDGE('',*,*,#2963,.T.);
#3825=ORIENTED_EDGE('',*,*,#2964,.T.);
#3826=ORIENTED_EDGE('',*,*,#2965,.T.);
#3827=ORIENTED_EDGE('',*,*,#2961,.F.);
#3828=ORIENTED_EDGE('',*,*,#2966,.T.);
#3829=ORIENTED_EDGE('',*,*,#2967,.T.);
#3830=ORIENTED_EDGE('',*,*,#2968,.T.);
#3831=ORIENTED_EDGE('',*,*,#2964,.F.);
#3832=ORIENTED_EDGE('',*,*,#2969,.T.);
#3833=ORIENTED_EDGE('',*,*,#2970,.T.);
#3834=ORIENTED_EDGE('',*,*,#2971,.T.);
#3835=ORIENTED_EDGE('',*,*,#2967,.F.);
#3836=ORIENTED_EDGE('',*,*,#2972,.T.);
#3837=ORIENTED_EDGE('',*,*,#2959,.T.);
#3838=ORIENTED_EDGE('',*,*,#2973,.T.);
#3839=ORIENTED_EDGE('',*,*,#2970,.F.);
#3840=ORIENTED_EDGE('',*,*,#2972,.F.);
#3841=ORIENTED_EDGE('',*,*,#2969,.F.);
#3842=ORIENTED_EDGE('',*,*,#2966,.F.);
#3843=ORIENTED_EDGE('',*,*,#2963,.F.);
#3844=ORIENTED_EDGE('',*,*,#2960,.F.);
#3845=ORIENTED_EDGE('',*,*,#2956,.F.);
#3846=ORIENTED_EDGE('',*,*,#2973,.F.);
#3847=ORIENTED_EDGE('',*,*,#2958,.F.);
#3848=ORIENTED_EDGE('',*,*,#2962,.F.);
#3849=ORIENTED_EDGE('',*,*,#2965,.F.);
#3850=ORIENTED_EDGE('',*,*,#2968,.F.);
#3851=ORIENTED_EDGE('',*,*,#2971,.F.);
#3852=ORIENTED_EDGE('',*,*,#2974,.F.);
#3853=ORIENTED_EDGE('',*,*,#2975,.F.);
#3854=ORIENTED_EDGE('',*,*,#2976,.F.);
#3855=ORIENTED_EDGE('',*,*,#2977,.T.);
#3856=ORIENTED_EDGE('',*,*,#2975,.T.);
#3857=ORIENTED_EDGE('',*,*,#2977,.F.);
#3858=ORIENTED_EDGE('',*,*,#2978,.F.);
#3859=ORIENTED_EDGE('',*,*,#2979,.T.);
#3860=ORIENTED_EDGE('',*,*,#2976,.T.);
#3861=ORIENTED_EDGE('',*,*,#2979,.F.);
#3862=ORIENTED_EDGE('',*,*,#2980,.F.);
#3863=ORIENTED_EDGE('',*,*,#2981,.T.);
#3864=ORIENTED_EDGE('',*,*,#2978,.T.);
#3865=ORIENTED_EDGE('',*,*,#2981,.F.);
#3866=ORIENTED_EDGE('',*,*,#2980,.T.);
#3867=ORIENTED_EDGE('',*,*,#2982,.F.);
#3868=ORIENTED_EDGE('',*,*,#2983,.F.);
#3869=ORIENTED_EDGE('',*,*,#2984,.T.);
#3870=ORIENTED_EDGE('',*,*,#2982,.T.);
#3871=ORIENTED_EDGE('',*,*,#2984,.F.);
#3872=ORIENTED_EDGE('',*,*,#2974,.T.);
#3873=ORIENTED_EDGE('',*,*,#2985,.T.);
#3874=ORIENTED_EDGE('',*,*,#2983,.T.);
#3875=ORIENTED_EDGE('',*,*,#2985,.F.);
#4640=CYLINDRICAL_SURFACE('',#5299,0.425);
#4641=CYLINDRICAL_SURFACE('',#5307,0.24505);
#4757=ADVANCED_FACE('',(#658),#445,.F.);
#4758=ADVANCED_FACE('',(#659),#446,.F.);
#4759=ADVANCED_FACE('',(#660),#447,.F.);
#4760=ADVANCED_FACE('',(#661),#448,.F.);
#4761=ADVANCED_FACE('',(#662),#449,.F.);
#4762=ADVANCED_FACE('',(#663),#450,.F.);
#4763=ADVANCED_FACE('',(#664),#451,.F.);
#4764=ADVANCED_FACE('',(#665),#452,.F.);
#4765=ADVANCED_FACE('',(#666),#453,.F.);
#4766=ADVANCED_FACE('',(#667),#454,.T.);
#4767=ADVANCED_FACE('',(#668),#211,.T.);
#4768=ADVANCED_FACE('',(#669),#4640,.T.);
#4769=ADVANCED_FACE('',(#670),#212,.T.);
#4770=ADVANCED_FACE('',(#671,#336),#455,.T.);
#4771=ADVANCED_FACE('',(#672),#213,.T.);
#4772=ADVANCED_FACE('',(#673),#4641,.T.);
#4944=CLOSED_SHELL('',(#4757,#4758,#4759,#4760,#4761,#4762,#4763,#4764));
#4945=CLOSED_SHELL('',(#4765,#4766,#4767,#4768,#4769,#4770,#4771,#4772));
#5284=AXIS2_PLACEMENT_3D('',#7535,#6067,#6068);
#5285=AXIS2_PLACEMENT_3D('',#7536,#6069,#6070);
#5286=AXIS2_PLACEMENT_3D('',#7545,#6075,#6076);
#5287=AXIS2_PLACEMENT_3D('',#7551,#6080,#6081);
#5288=AXIS2_PLACEMENT_3D('',#7557,#6085,#6086);
#5289=AXIS2_PLACEMENT_3D('',#7563,#6090,#6091);
#5290=AXIS2_PLACEMENT_3D('',#7569,#6095,#6096);
#5291=AXIS2_PLACEMENT_3D('',#7572,#6099,#6100);
#5292=AXIS2_PLACEMENT_3D('',#7573,#6101,#6102);
#5293=AXIS2_PLACEMENT_3D('',#7574,#6103,#6104);
#5294=AXIS2_PLACEMENT_3D('',#7576,#6105,#6106);
#5295=AXIS2_PLACEMENT_3D('',#7577,#6107,#6108);
#5296=AXIS2_PLACEMENT_3D('',#7579,#6109,#6110);
#5297=AXIS2_PLACEMENT_3D('',#7580,#6111,#6112);
#5298=AXIS2_PLACEMENT_3D('',#7582,#6113,#6114);
#5299=AXIS2_PLACEMENT_3D('',#7584,#6116,#6117);
#5300=AXIS2_PLACEMENT_3D('',#7586,#6118,#6119);
#5301=AXIS2_PLACEMENT_3D('',#7588,#6121,#6122);
#5302=AXIS2_PLACEMENT_3D('',#7590,#6123,#6124);
#5303=AXIS2_PLACEMENT_3D('',#7592,#6126,#6127);
#5304=AXIS2_PLACEMENT_3D('',#7594,#6128,#6129);
#5305=AXIS2_PLACEMENT_3D('',#7595,#6130,#6131);
#5306=AXIS2_PLACEMENT_3D('',#7597,#6132,#6133);
#5307=AXIS2_PLACEMENT_3D('',#7599,#6135,#6136);
#6067=DIRECTION('axis',(0.,0.,1.));
#6068=DIRECTION('refdir',(1.,0.,0.));
#6069=DIRECTION('center_axis',(0.866025403784439,0.,-0.5));
#6070=DIRECTION('ref_axis',(0.5,0.,0.866025403784439));
#6071=DIRECTION('',(-0.5,0.,-0.866025403784439));
#6072=DIRECTION('',(0.,-1.,0.));
#6073=DIRECTION('',(0.5,0.,0.866025403784439));
#6074=DIRECTION('',(0.,-1.,0.));
#6075=DIRECTION('center_axis',(1.20185167898973E-16,0.,-1.));
#6076=DIRECTION('ref_axis',(1.,0.,1.20185167898973E-16));
#6077=DIRECTION('',(-1.,0.,-1.20185167898973E-16));
#6078=DIRECTION('',(0.,-1.,0.));
#6079=DIRECTION('',(1.,0.,1.20185167898973E-16));
#6080=DIRECTION('center_axis',(-0.866025403784439,0.,-0.5));
#6081=DIRECTION('ref_axis',(0.5,0.,-0.866025403784439));
#6082=DIRECTION('',(-0.5,0.,0.866025403784439));
#6083=DIRECTION('',(0.,-1.,0.));
#6084=DIRECTION('',(0.5,0.,-0.866025403784439));
#6085=DIRECTION('center_axis',(-0.866025403784439,0.,0.5));
#6086=DIRECTION('ref_axis',(-0.5,0.,-0.866025403784439));
#6087=DIRECTION('',(0.5,0.,0.866025403784439));
#6088=DIRECTION('',(0.,-1.,0.));
#6089=DIRECTION('',(-0.5,0.,-0.866025403784439));
#6090=DIRECTION('center_axis',(-2.40370335797945E-16,0.,1.));
#6091=DIRECTION('ref_axis',(-1.,0.,-2.40370335797945E-16));
#6092=DIRECTION('',(1.,0.,2.40370335797945E-16));
#6093=DIRECTION('',(0.,-1.,0.));
#6094=DIRECTION('',(-1.,0.,-2.40370335797945E-16));
#6095=DIRECTION('center_axis',(0.866025403784439,0.,0.5));
#6096=DIRECTION('ref_axis',(-0.5,0.,0.866025403784439));
#6097=DIRECTION('',(0.5,0.,-0.866025403784439));
#6098=DIRECTION('',(-0.5,0.,0.866025403784439));
#6099=DIRECTION('center_axis',(0.,1.,0.));
#6100=DIRECTION('ref_axis',(1.,0.,0.));
#6101=DIRECTION('center_axis',(0.,-1.,0.));
#6102=DIRECTION('ref_axis',(0.,0.,-1.));
#6103=DIRECTION('center_axis',(0.,1.,0.));
#6104=DIRECTION('ref_axis',(1.,0.,0.));
#6105=DIRECTION('center_axis',(0.,1.,0.));
#6106=DIRECTION('ref_axis',(1.,0.,0.));
#6107=DIRECTION('center_axis',(0.,1.,0.));
#6108=DIRECTION('ref_axis',(0.,0.,1.));
#6109=DIRECTION('center_axis',(0.,-1.,0.));
#6110=DIRECTION('ref_axis',(1.,0.,0.));
#6111=DIRECTION('center_axis',(0.,-1.,0.));
#6112=DIRECTION('ref_axis',(1.,0.,0.));
#6113=DIRECTION('center_axis',(0.,-1.,0.));
#6114=DIRECTION('ref_axis',(1.,0.,0.));
#6115=DIRECTION('',(0.707106781186548,0.707106781186547,8.65956056235493E-17));
#6116=DIRECTION('center_axis',(0.,-1.,0.));
#6117=DIRECTION('ref_axis',(1.,0.,0.));
#6118=DIRECTION('center_axis',(0.,-1.,0.));
#6119=DIRECTION('ref_axis',(1.,0.,0.));
#6120=DIRECTION('',(0.,1.,0.));
#6121=DIRECTION('center_axis',(0.,1.,0.));
#6122=DIRECTION('ref_axis',(1.,0.,0.));
#6123=DIRECTION('center_axis',(0.,-1.,0.));
#6124=DIRECTION('ref_axis',(1.,0.,0.));
#6125=DIRECTION('',(-0.707106781186547,0.707106781186548,-8.65956056235493E-17));
#6126=DIRECTION('center_axis',(0.,-1.,0.));
#6127=DIRECTION('ref_axis',(0.,0.,-1.));
#6128=DIRECTION('center_axis',(0.,-1.,0.));
#6129=DIRECTION('ref_axis',(1.,0.,0.));
#6130=DIRECTION('center_axis',(0.,1.,0.));
#6131=DIRECTION('ref_axis',(1.,0.,0.));
#6132=DIRECTION('center_axis',(0.,1.,0.));
#6133=DIRECTION('ref_axis',(1.,0.,0.));
#6134=DIRECTION('',(-0.447213595499958,0.894427190999916,-5.47678698264203E-17));
#6135=DIRECTION('center_axis',(0.,-1.,0.));
#6136=DIRECTION('ref_axis',(1.,0.,0.));
#6137=DIRECTION('',(0.,1.,0.));
#7535=CARTESIAN_POINT('',(0.,0.,0.));
#7536=CARTESIAN_POINT('Origin',(0.115470053837925,-0.5,-0.2));
#7537=CARTESIAN_POINT('',(0.23094010767585,-0.5,0.));
#7538=CARTESIAN_POINT('',(0.115470053837925,-0.5,-0.2));
#7539=CARTESIAN_POINT('',(0.23094010767585,-0.5,0.));
#7540=CARTESIAN_POINT('',(0.115470053837925,-0.8,-0.2));
#7541=CARTESIAN_POINT('',(0.115470053837925,-0.5,-0.2));
#7542=CARTESIAN_POINT('',(0.23094010767585,-0.8,0.));
#7543=CARTESIAN_POINT('',(0.23094010767585,-0.8,0.));
#7544=CARTESIAN_POINT('',(0.23094010767585,-0.5,0.));
#7545=CARTESIAN_POINT('Origin',(-0.115470053837925,-0.5,-0.2));
#7546=CARTESIAN_POINT('',(-0.115470053837925,-0.5,-0.2));
#7547=CARTESIAN_POINT('',(0.115470053837925,-0.5,-0.2));
#7548=CARTESIAN_POINT('',(-0.115470053837925,-0.8,-0.2));
#7549=CARTESIAN_POINT('',(-0.115470053837925,-0.5,-0.2));
#7550=CARTESIAN_POINT('',(0.115470053837925,-0.8,-0.2));
#7551=CARTESIAN_POINT('Origin',(-0.23094010767585,-0.5,-2.77555756156289E-17));
#7552=CARTESIAN_POINT('',(-0.23094010767585,-0.5,-2.82820063659975E-17));
#7553=CARTESIAN_POINT('',(-0.115470053837925,-0.5,-0.2));
#7554=CARTESIAN_POINT('',(-0.23094010767585,-0.8,-2.77555756156289E-17));
#7555=CARTESIAN_POINT('',(-0.23094010767585,-0.5,-2.82820063659975E-17));
#7556=CARTESIAN_POINT('',(-0.115470053837925,-0.8,-0.2));
#7557=CARTESIAN_POINT('Origin',(-0.115470053837925,-0.5,0.2));
#7558=CARTESIAN_POINT('',(-0.115470053837925,-0.5,0.2));
#7559=CARTESIAN_POINT('',(-0.23094010767585,-0.5,-2.82820063659975E-17));
#7560=CARTESIAN_POINT('',(-0.115470053837925,-0.8,0.2));
#7561=CARTESIAN_POINT('',(-0.115470053837925,-0.5,0.2));
#7562=CARTESIAN_POINT('',(-0.23094010767585,-0.8,-2.82820063659975E-17));
#7563=CARTESIAN_POINT('Origin',(0.115470053837925,-0.5,0.2));
#7564=CARTESIAN_POINT('',(0.115470053837925,-0.5,0.2));
#7565=CARTESIAN_POINT('',(-0.115470053837925,-0.5,0.2));
#7566=CARTESIAN_POINT('',(0.115470053837925,-0.8,0.2));
#7567=CARTESIAN_POINT('',(0.115470053837925,-0.5,0.2));
#7568=CARTESIAN_POINT('',(-0.115470053837925,-0.8,0.2));
#7569=CARTESIAN_POINT('Origin',(0.23094010767585,-0.5,0.));
#7570=CARTESIAN_POINT('',(0.115470053837925,-0.5,0.2));
#7571=CARTESIAN_POINT('',(0.115470053837925,-0.8,0.2));
#7572=CARTESIAN_POINT('Origin',(0.,-0.5,0.));
#7573=CARTESIAN_POINT('Origin',(0.,-0.8,0.));
#7574=CARTESIAN_POINT('Origin',(0.,-1.4,0.));
#7575=CARTESIAN_POINT('',(-0.24505,-1.4,3.00099698131059E-17));
#7576=CARTESIAN_POINT('Origin',(0.,-1.4,0.));
#7577=CARTESIAN_POINT('Origin',(0.375,0.5,0.));
#7578=CARTESIAN_POINT('',(-0.375,0.5,-4.59242549680257E-17));
#7579=CARTESIAN_POINT('Origin',(0.,0.5,0.));
#7580=CARTESIAN_POINT('Origin',(0.,0.475,0.));
#7581=CARTESIAN_POINT('',(-0.425,0.45,-5.20474889637625E-17));
#7582=CARTESIAN_POINT('Origin',(0.,0.45,0.));
#7583=CARTESIAN_POINT('',(-0.4,0.475,-4.89858719658941E-17));
#7584=CARTESIAN_POINT('Origin',(0.,0.24,0.));
#7585=CARTESIAN_POINT('',(-0.425,0.0299999999999998,-5.20474889637625E-17));
#7586=CARTESIAN_POINT('Origin',(0.,0.0299999999999998,0.));
#7587=CARTESIAN_POINT('',(-0.425,0.24,-5.20474889637625E-17));
#7588=CARTESIAN_POINT('Origin',(0.,0.0150000000000001,0.));
#7589=CARTESIAN_POINT('',(-0.395,4.85722573273506E-17,-4.83735485663204E-17));
#7590=CARTESIAN_POINT('Origin',(0.,0.,0.));
#7591=CARTESIAN_POINT('',(-0.41,0.0150000000000001,-5.02105187650415E-17));
#7592=CARTESIAN_POINT('Origin',(0.27,0.,0.));
#7593=CARTESIAN_POINT('',(-0.27,0.,-3.30654635769785E-17));
#7594=CARTESIAN_POINT('Origin',(0.,0.,0.));
#7595=CARTESIAN_POINT('Origin',(0.,-0.02,0.));
#7596=CARTESIAN_POINT('',(-0.24505,-0.0498999999999999,3.00099698131059E-17));
#7597=CARTESIAN_POINT('Origin',(0.,-0.0498999999999999,0.));
#7598=CARTESIAN_POINT('',(-0.26,-0.02,-3.18408167778312E-17));
#7599=CARTESIAN_POINT('Origin',(0.,-0.995,0.));
#7600=CARTESIAN_POINT('',(-0.24505,-0.995,-3.00099698131059E-17));
#8459=UNCERTAINTY_MEASURE_WITH_UNIT(LENGTH_MEASURE(0.001),#8500,
'DISTANCE_ACCURACY_VALUE',
'Maximum model space distance between geometric entities at asserted c
onnectivities');
#8476=UNCERTAINTY_MEASURE_WITH_UNIT(LENGTH_MEASURE(0.001),#8500,
'DISTANCE_ACCURACY_VALUE',
'Maximum model space distance between geometric entities at asserted c
onnectivities');
#8482=(
GEOMETRIC_REPRESENTATION_CONTEXT(3)
GLOBAL_UNCERTAINTY_ASSIGNED_CONTEXT((#8459))
GLOBAL_UNIT_ASSIGNED_CONTEXT((#8500,#8502,#8503))
REPRESENTATION_CONTEXT('','3D')
);
#8499=(
GEOMETRIC_REPRESENTATION_CONTEXT(3)
GLOBAL_UNCERTAINTY_ASSIGNED_CONTEXT((#8476))
GLOBAL_UNIT_ASSIGNED_CONTEXT((#8500,#8502,#8503))
REPRESENTATION_CONTEXT('','3D')
);
#8500=(
LENGTH_UNIT()
NAMED_UNIT(*)
SI_UNIT(.CENTI.,.METRE.)
);
#8502=(
NAMED_UNIT(*)
PLANE_ANGLE_UNIT()
SI_UNIT($,.RADIAN.)
);
#8503=(
NAMED_UNIT(*)
SI_UNIT($,.STERADIAN.)
SOLID_ANGLE_UNIT()
);
#8509=SHAPE_DEFINITION_REPRESENTATION(#8531,#8603);
#8531=PRODUCT_DEFINITION_SHAPE('',$,#8626);
#8603=SHAPE_REPRESENTATION('',(#5284),#8482);
#8620=PRODUCT_DEFINITION_CONTEXT('part definition',#8688,'design');
#8626=PRODUCT_DEFINITION('M5x14 Cap Screw','M5x14 Cap Screw',#8648,#8620);
#8648=PRODUCT_DEFINITION_FORMATION('',$,#8695);
#8688=APPLICATION_CONTEXT(
'Core Data for Automotive Mechanical Design Process');
#8689=PRODUCT_CONTEXT('part definition',#8688,'mechanical');
#8695=PRODUCT('M5x14 Cap Screw','M5x14 Cap Screw','M5x14 Cap Screw',(#8689));
#8789=COLOUR_RGB('Black',0.12,0.14,0.17);
#8790=FILL_AREA_STYLE_COLOUR('',#8789);
#8791=FILL_AREA_STYLE('',(#8790));
#8792=SURFACE_STYLE_FILL_AREA(#8791);
#8793=SURFACE_SIDE_STYLE('',(#8792));
#8794=SURFACE_STYLE_USAGE(.BOTH.,#8793);
#8795=PRESENTATION_STYLE_ASSIGNMENT((#8794));
ENDSEC;
END-ISO-10303-21;
